ISO-10303-21;
HEADER;
/* Generated by software containing ST-Developer
 * from STEP Tools, Inc. (www.steptools.com) 
 */

FILE_DESCRIPTION(
/* description */ ('Cylinder foot and clevis mount kit'),
/* implementation_level */ '2;1');

FILE_NAME(
/* name */ 'Cap Screw - M5x20.step',
/* time_stamp */ '2026-10-27T20:10:43-07:00',
/* author */ (''),
/* organization */ (''),
/* preprocessor_version */ 'ST-DEVELOPER v20.2',
/* originating_system */ 'Autodesk Translation Framework v15.17.0.0',
/* authorisation */ '');

FILE_SCHEMA (('AUTOMOTIVE_DESIGN { 1 0 10303 214 3 1 1 }'));
ENDSEC;

DATA;
#10=MECHANICAL_DESIGN_GEOMETRIC_PRESENTATION_REPRESENTATION('',(#348),#9102);
#259=ORIENTED_CLOSED_SHELL('',*,#4935,.F.);
#261=BREP_WITH_VOIDS('Body1',#4934,(#259));
#267=CONICAL_SURFACE('',#5571,0.4,0.785398163397448);
#268=CONICAL_SURFACE('',#5575,0.41,0.785398163397448);
#269=CONICAL_SURFACE('',#5579,0.26,0.463647609000806);
#270=CONICAL_SURFACE('',#5583,0.225,0.785398163397448);
#292=SHAPE_REPRESENTATION_RELATIONSHIP('SRR','None',#9239,#320);
#320=ADVANCED_BREP_SHAPE_REPRESENTATION('',(#261),#9082);
#348=STYLED_ITEM('',(#9467),#261);
#456=FACE_BOUND('',#1229,.T.);
#605=PLANE('',#5569);
#606=PLANE('',#5577);
#607=PLANE('',#5585);
#608=PLANE('',#5586);
#609=PLANE('',#5587);
#610=PLANE('',#5588);
#611=PLANE('',#5589);
#612=PLANE('',#5590);
#613=PLANE('',#5591);
#614=PLANE('',#5592);
#615=PLANE('',#5593);
#854=FACE_OUTER_BOUND('',#1224,.T.);
#855=FACE_OUTER_BOUND('',#1225,.T.);
#856=FACE_OUTER_BOUND('',#1226,.T.);
#857=FACE_OUTER_BOUND('',#1227,.T.);
#858=FACE_OUTER_BOUND('',#1228,.T.);
#859=FACE_OUTER_BOUND('',#1230,.T.);
#860=FACE_OUTER_BOUND('',#1231,.T.);
#861=FACE_OUTER_BOUND('',#1232,.T.);
#862=FACE_OUTER_BOUND('',#1233,.T.);
#863=FACE_OUTER_BOUND('',#1234,.T.);
#864=FACE_OUTER_BOUND('',#1235,.T.);
#865=FACE_OUTER_BOUND('',#1236,.T.);
#866=FACE_OUTER_BOUND('',#1237,.T.);
#867=FACE_OUTER_BOUND('',#1238,.T.);
#868=FACE_OUTER_BOUND('',#1239,.T.);
#869=FACE_OUTER_BOUND('',#1240,.T.);
#870=FACE_OUTER_BOUND('',#1241,.T.);
#1224=EDGE_LOOP('',(#3957));
#1225=EDGE_LOOP('',(#3958,#3959,#3960,#3961));
#1226=EDGE_LOOP('',(#3962,#3963,#3964,#3965));
#1227=EDGE_LOOP('',(#3966,#3967,#3968,#3969));
#1228=EDGE_LOOP('',(#3970));
#1229=EDGE_LOOP('',(#3971));
#1230=EDGE_LOOP('',(#3972,#3973,#3974,#3975));
#1231=EDGE_LOOP('',(#3976,#3977,#3978,#3979));
#1232=EDGE_LOOP('',(#3980,#3981,#3982,#3983));
#1233=EDGE_LOOP('',(#3984));
#1234=EDGE_LOOP('',(#3985,#3986,#3987,#3988));
#1235=EDGE_LOOP('',(#3989,#3990,#3991,#3992));
#1236=EDGE_LOOP('',(#3993,#3994,#3995,#3996));
#1237=EDGE_LOOP('',(#3997,#3998,#3999,#4000));
#1238=EDGE_LOOP('',(#4001,#4002,#4003,#4004));
#1239=EDGE_LOOP('',(#4005,#4006,#4007,#4008));
#1240=EDGE_LOOP('',(#4009,#4010,#4011,#4012,#4013,#4014));
#1241=EDGE_LOOP('',(#4015,#4016,#4017,#4018,#4019,#4020));
#1597=LINE('',#8197,#1946);
#1598=LINE('',#8201,#1947);
#1599=LINE('',#8205,#1948);
#1600=LINE('',#8212,#1949);
#1601=LINE('',#8216,#1950);
#1602=LINE('',#8220,#1951);
#1603=LINE('',#8225,#1952);
#1604=LINE('',#8227,#1953);
#1605=LINE('',#8229,#1954);
#1606=LINE('',#8230,#1955);
#1607=LINE('',#8233,#1956);
#1608=LINE('',#8235,#1957);
#1609=LINE('',#8236,#1958);
#1610=LINE('',#8239,#1959);
#1611=LINE('',#8241,#1960);
#1612=LINE('',#8242,#1961);
#1613=LINE('',#8245,#1962);
#1614=LINE('',#8247,#1963);
#1615=LINE('',#8248,#1964);
#1616=LINE('',#8251,#1965);
#1617=LINE('',#8253,#1966);
#1618=LINE('',#8254,#1967);
#1619=LINE('',#8256,#1968);
#1620=LINE('',#8257,#1969);
#1946=VECTOR('',#6698,0.4);
#1947=VECTOR('',#6703,0.425);
#1948=VECTOR('',#6708,0.41);
#1949=VECTOR('',#6717,0.26);
#1950=VECTOR('',#6722,0.25);
#1951=VECTOR('',#6727,0.225);
#1952=VECTOR('',#6732,1.);
#1953=VECTOR('',#6733,1.);
#1954=VECTOR('',#6734,1.);
#1955=VECTOR('',#6735,1.);
#1956=VECTOR('',#6738,1.);
#1957=VECTOR('',#6739,1.);
#1958=VECTOR('',#6740,1.);
#1959=VECTOR('',#6743,1.);
#1960=VECTOR('',#6744,1.);
#1961=VECTOR('',#6745,1.);
#1962=VECTOR('',#6748,1.);
#1963=VECTOR('',#6749,1.);
#1964=VECTOR('',#6750,1.);
#1965=VECTOR('',#6753,1.);
#1966=VECTOR('',#6754,1.);
#1967=VECTOR('',#6755,1.);
#1968=VECTOR('',#6758,1.);
#1969=VECTOR('',#6759,1.);
#2228=CIRCLE('',#5570,0.375);
#2229=CIRCLE('',#5572,0.425);
#2230=CIRCLE('',#5574,0.425);
#2231=CIRCLE('',#5576,0.395);
#2232=CIRCLE('',#5578,0.27);
#2233=CIRCLE('',#5580,0.24505);
#2234=CIRCLE('',#5582,0.24505);
#2235=CIRCLE('',#5584,0.2);
#2530=VERTEX_POINT('',#8192);
#2531=VERTEX_POINT('',#8195);
#2532=VERTEX_POINT('',#8199);
#2533=VERTEX_POINT('',#8203);
#2534=VERTEX_POINT('',#8207);
#2535=VERTEX_POINT('',#8210);
#2536=VERTEX_POINT('',#8214);
#2537=VERTEX_POINT('',#8218);
#2538=VERTEX_POINT('',#8223);
#2539=VERTEX_POINT('',#8224);
#2540=VERTEX_POINT('',#8226);
#2541=VERTEX_POINT('',#8228);
#2542=VERTEX_POINT('',#8232);
#2543=VERTEX_POINT('',#8234);
#2544=VERTEX_POINT('',#8238);
#2545=VERTEX_POINT('',#8240);
#2546=VERTEX_POINT('',#8244);
#2547=VERTEX_POINT('',#8246);
#2548=VERTEX_POINT('',#8250);
#2549=VERTEX_POINT('',#8252);
#3033=EDGE_CURVE('',#2530,#2530,#2228,.T.);
#3034=EDGE_CURVE('',#2531,#2531,#2229,.T.);
#3035=EDGE_CURVE('',#2531,#2530,#1597,.T.);
#3036=EDGE_CURVE('',#2532,#2532,#2230,.T.);
#3037=EDGE_CURVE('',#2532,#2531,#1598,.T.);
#3038=EDGE_CURVE('',#2533,#2533,#2231,.T.);
#3039=EDGE_CURVE('',#2533,#2532,#1599,.T.);
#3040=EDGE_CURVE('',#2534,#2534,#2232,.T.);
#3041=EDGE_CURVE('',#2535,#2535,#2233,.F.);
#3042=EDGE_CURVE('',#2535,#2534,#1600,.T.);
#3043=EDGE_CURVE('',#2536,#2536,#2234,.F.);
#3044=EDGE_CURVE('',#2536,#2535,#1601,.T.);
#3045=EDGE_CURVE('',#2537,#2537,#2235,.T.);
#3046=EDGE_CURVE('',#2537,#2536,#1602,.T.);
#3047=EDGE_CURVE('',#2538,#2539,#1603,.T.);
#3048=EDGE_CURVE('',#2539,#2540,#1604,.T.);
#3049=EDGE_CURVE('',#2540,#2541,#1605,.T.);
#3050=EDGE_CURVE('',#2538,#2541,#1606,.T.);
#3051=EDGE_CURVE('',#2539,#2542,#1607,.T.);
#3052=EDGE_CURVE('',#2542,#2543,#1608,.T.);
#3053=EDGE_CURVE('',#2543,#2540,#1609,.T.);
#3054=EDGE_CURVE('',#2542,#2544,#1610,.T.);
#3055=EDGE_CURVE('',#2544,#2545,#1611,.T.);
#3056=EDGE_CURVE('',#2545,#2543,#1612,.T.);
#3057=EDGE_CURVE('',#2544,#2546,#1613,.T.);
#3058=EDGE_CURVE('',#2546,#2547,#1614,.T.);
#3059=EDGE_CURVE('',#2547,#2545,#1615,.T.);
#3060=EDGE_CURVE('',#2546,#2548,#1616,.T.);
#3061=EDGE_CURVE('',#2548,#2549,#1617,.T.);
#3062=EDGE_CURVE('',#2549,#2547,#1618,.T.);
#3063=EDGE_CURVE('',#2548,#2538,#1619,.T.);
#3064=EDGE_CURVE('',#2541,#2549,#1620,.T.);
#3957=ORIENTED_EDGE('',*,*,#3033,.F.);
#3958=ORIENTED_EDGE('',*,*,#3034,.F.);
#3959=ORIENTED_EDGE('',*,*,#3035,.T.);
#3960=ORIENTED_EDGE('',*,*,#3033,.T.);
#3961=ORIENTED_EDGE('',*,*,#3035,.F.);
#3962=ORIENTED_EDGE('',*,*,#3036,.F.);
#3963=ORIENTED_EDGE('',*,*,#3037,.T.);
#3964=ORIENTED_EDGE('',*,*,#3034,.T.);
#3965=ORIENTED_EDGE('',*,*,#3037,.F.);
#3966=ORIENTED_EDGE('',*,*,#3038,.F.);
#3967=ORIENTED_EDGE('',*,*,#3039,.T.);
#3968=ORIENTED_EDGE('',*,*,#3036,.T.);
#3969=ORIENTED_EDGE('',*,*,#3039,.F.);
#3970=ORIENTED_EDGE('',*,*,#3038,.T.);
#3971=ORIENTED_EDGE('',*,*,#3040,.F.);
#3972=ORIENTED_EDGE('',*,*,#3041,.F.);
#3973=ORIENTED_EDGE('',*,*,#3042,.T.);
#3974=ORIENTED_EDGE('',*,*,#3040,.T.);
#3975=ORIENTED_EDGE('',*,*,#3042,.F.);
#3976=ORIENTED_EDGE('',*,*,#3043,.F.);
#3977=ORIENTED_EDGE('',*,*,#3044,.T.);
#3978=ORIENTED_EDGE('',*,*,#3041,.T.);
#3979=ORIENTED_EDGE('',*,*,#3044,.F.);
#3980=ORIENTED_EDGE('',*,*,#3045,.F.);
#3981=ORIENTED_EDGE('',*,*,#3046,.T.);
#3982=ORIENTED_EDGE('',*,*,#3043,.T.);
#3983=ORIENTED_EDGE('',*,*,#3046,.F.);
#3984=ORIENTED_EDGE('',*,*,#3045,.T.);
#3985=ORIENTED_EDGE('',*,*,#3047,.T.);
#3986=ORIENTED_EDGE('',*,*,#3048,.T.);
#3987=ORIENTED_EDGE('',*,*,#3049,.T.);
#3988=ORIENTED_EDGE('',*,*,#3050,.F.);
#3989=ORIENTED_EDGE('',*,*,#3051,.T.);
#3990=ORIENTED_EDGE('',*,*,#3052,.T.);
#3991=ORIENTED_EDGE('',*,*,#3053,.T.);
#3992=ORIENTED_EDGE('',*,*,#3048,.F.);
#3993=ORIENTED_EDGE('',*,*,#3054,.T.);
#3994=ORIENTED_EDGE('',*,*,#3055,.T.);
#3995=ORIENTED_EDGE('',*,*,#3056,.T.);
#3996=ORIENTED_EDGE('',*,*,#3052,.F.);
#3997=ORIENTED_EDGE('',*,*,#3057,.T.);
#3998=ORIENTED_EDGE('',*,*,#3058,.T.);
#3999=ORIENTED_EDGE('',*,*,#3059,.T.);
#4000=ORIENTED_EDGE('',*,*,#3055,.F.);
#4001=ORIENTED_EDGE('',*,*,#3060,.T.);
#4002=ORIENTED_EDGE('',*,*,#3061,.T.);
#4003=ORIENTED_EDGE('',*,*,#3062,.T.);
#4004=ORIENTED_EDGE('',*,*,#3058,.F.);
#4005=ORIENTED_EDGE('',*,*,#3063,.T.);
#4006=ORIENTED_EDGE('',*,*,#3050,.T.);
#4007=ORIENTED_EDGE('',*,*,#3064,.T.);
#4008=ORIENTED_EDGE('',*,*,#3061,.F.);
#4009=ORIENTED_EDGE('',*,*,#3063,.F.);
#4010=ORIENTED_EDGE('',*,*,#3060,.F.);
#4011=ORIENTED_EDGE('',*,*,#3057,.F.);
#4012=ORIENTED_EDGE('',*,*,#3054,.F.);
#4013=ORIENTED_EDGE('',*,*,#3051,.F.);
#4014=ORIENTED_EDGE('',*,*,#3047,.F.);
#4015=ORIENTED_EDGE('',*,*,#3064,.F.);
#4016=ORIENTED_EDGE('',*,*,#3049,.F.);
#4017=ORIENTED_EDGE('',*,*,#3053,.F.);
#4018=ORIENTED_EDGE('',*,*,#3056,.F.);
#4019=ORIENTED_EDGE('',*,*,#3059,.F.);
#4020=ORIENTED_EDGE('',*,*,#3062,.F.);
#4580=CYLINDRICAL_SURFACE('',#5573,0.425);
#4581=CYLINDRICAL_SURFACE('',#5581,0.24505);
#4777=ADVANCED_FACE('',(#854),#605,.T.);
#4778=ADVANCED_FACE('',(#855),#267,.T.);
#4779=ADVANCED_FACE('',(#856),#4580,.T.);
#4780=ADVANCED_FACE('',(#857),#268,.T.);
#4781=ADVANCED_FACE('',(#858,#456),#606,.T.);
#4782=ADVANCED_FACE('',(#859),#269,.T.);
#4783=ADVANCED_FACE('',(#860),#4581,.T.);
#4784=ADVANCED_FACE('',(#861),#270,.T.);
#4785=ADVANCED_FACE('',(#862),#607,.T.);
#4786=ADVANCED_FACE('',(#863),#608,.F.);
#4787=ADVANCED_FACE('',(#864),#609,.F.);
#4788=ADVANCED_FACE('',(#865),#610,.F.);
#4789=ADVANCED_FACE('',(#866),#611,.F.);
#4790=ADVANCED_FACE('',(#867),#612,.F.);
#4791=ADVANCED_FACE('',(#868),#613,.F.);
#4792=ADVANCED_FACE('',(#869),#614,.F.);
#4793=ADVANCED_FACE('',(#870),#615,.F.);
#4934=CLOSED_SHELL('',(#4777,#4778,#4779,#4780,#4781,#4782,#4783,#4784,
#4785));
#4935=CLOSED_SHELL('',(#4786,#4787,#4788,#4789,#4790,#4791,#4792,#4793));
#5568=AXIS2_PLACEMENT_3D('',#8190,#6688,#6689);
#5569=AXIS2_PLACEMENT_3D('',#8191,#6690,#6691);
#5570=AXIS2_PLACEMENT_3D('',#8193,#6692,#6693);
#5571=AXIS2_PLACEMENT_3D('',#8194,#6694,#6695);
#5572=AXIS2_PLACEMENT_3D('',#8196,#6696,#6697);
#5573=AXIS2_PLACEMENT_3D('',#8198,#6699,#6700);
#5574=AXIS2_PLACEMENT_3D('',#8200,#6701,#6702);
#5575=AXIS2_PLACEMENT_3D('',#8202,#6704,#6705);
#5576=AXIS2_PLACEMENT_3D('',#8204,#6706,#6707);
#5577=AXIS2_PLACEMENT_3D('',#8206,#6709,#6710);
#5578=AXIS2_PLACEMENT_3D('',#8208,#6711,#6712);
#5579=AXIS2_PLACEMENT_3D('',#8209,#6713,#6714);
#5580=AXIS2_PLACEMENT_3D('',#8211,#6715,#6716);
#5581=AXIS2_PLACEMENT_3D('',#8213,#6718,#6719);
#5582=AXIS2_PLACEMENT_3D('',#8215,#6720,#6721);
#5583=AXIS2_PLACEMENT_3D('',#8217,#6723,#6724);
#5584=AXIS2_PLACEMENT_3D('',#8219,#6725,#6726);
#5585=AXIS2_PLACEMENT_3D('',#8221,#6728,#6729);
#5586=AXIS2_PLACEMENT_3D('',#8222,#6730,#6731);
#5587=AXIS2_PLACEMENT_3D('',#8231,#6736,#6737);
#5588=AXIS2_PLACEMENT_3D('',#8237,#6741,#6742);
#5589=AXIS2_PLACEMENT_3D('',#8243,#6746,#6747);
#5590=AXIS2_PLACEMENT_3D('',#8249,#6751,#6752);
#5591=AXIS2_PLACEMENT_3D('',#8255,#6756,#6757);
#5592=AXIS2_PLACEMENT_3D('',#8258,#6760,#6761);
#5593=AXIS2_PLACEMENT_3D('',#8259,#6762,#6763);
#6688=DIRECTION('axis',(0.,0.,1.));
#6689=DIRECTION('refdir',(1.,0.,0.));
#6690=DIRECTION('center_axis',(0.,1.,0.));
#6691=DIRECTION('ref_axis',(0.,0.,1.));
#6692=DIRECTION('center_axis',(0.,-1.,0.));
#6693=DIRECTION('ref_axis',(1.,0.,0.));
#6694=DIRECTION('center_axis',(0.,-1.,0.));
#6695=DIRECTION('ref_axis',(1.,0.,0.));
#6696=DIRECTION('center_axis',(0.,-1.,0.));
#6697=DIRECTION('ref_axis',(1.,0.,0.));
#6698=DIRECTION('',(0.707106781186548,0.707106781186547,8.65956056235493E-17));
#6699=DIRECTION('center_axis',(0.,-1.,0.));
#6700=DIRECTION('ref_axis',(1.,0.,0.));
#6701=DIRECTION('center_axis',(0.,-1.,0.));
#6702=DIRECTION('ref_axis',(1.,0.,0.));
#6703=DIRECTION('',(0.,1.,0.));
#6704=DIRECTION('center_axis',(0.,1.,0.));
#6705=DIRECTION('ref_axis',(1.,0.,0.));
#6706=DIRECTION('center_axis',(0.,-1.,0.));
#6707=DIRECTION('ref_axis',(1.,0.,0.));
#6708=DIRECTION('',(-0.707106781186547,0.707106781186548,-8.65956056235493E-17));
#6709=DIRECTION('center_axis',(0.,-1.,0.));
#6710=DIRECTION('ref_axis',(0.,0.,-1.));
#6711=DIRECTION('center_axis',(0.,-1.,0.));
#6712=DIRECTION('ref_axis',(1.,0.,0.));
#6713=DIRECTION('center_axis',(0.,1.,0.));
#6714=DIRECTION('ref_axis',(1.,0.,0.));
#6715=DIRECTION('center_axis',(0.,1.,0.));
#6716=DIRECTION('ref_axis',(1.,0.,0.));
#6717=DIRECTION('',(-0.447213595499958,0.894427190999916,-5.47678698264203E-17));
#6718=DIRECTION('center_axis',(0.,-1.,0.));
#6719=DIRECTION('ref_axis',(1.,0.,0.));
#6720=DIRECTION('center_axis',(0.,1.,0.));
#6721=DIRECTION('ref_axis',(1.,0.,0.));
#6722=DIRECTION('',(0.,1.,0.));
#6723=DIRECTION('center_axis',(0.,1.,0.));
#6724=DIRECTION('ref_axis',(1.,0.,0.));
#6725=DIRECTION('center_axis',(0.,-1.,0.));
#6726=DIRECTION('ref_axis',(1.,0.,0.));
#6727=DIRECTION('',(-0.707106781186547,0.707106781186548,-8.65956056235493E-17));
#6728=DIRECTION('center_axis',(0.,-1.,0.));
#6729=DIRECTION('ref_axis',(0.,0.,-1.));
#6730=DIRECTION('center_axis',(0.866025403784439,0.,-0.5));
#6731=DIRECTION('ref_axis',(0.5,0.,0.866025403784439));
#6732=DIRECTION('',(-0.5,0.,-0.866025403784439));
#6733=DIRECTION('',(0.,-1.,0.));
#6734=DIRECTION('',(0.5,0.,0.866025403784439));
#6735=DIRECTION('',(0.,-1.,0.));
#6736=DIRECTION('center_axis',(1.20185167898973E-16,0.,-1.));
#6737=DIRECTION('ref_axis',(1.,0.,1.20185167898973E-16));
#6738=DIRECTION('',(-1.,0.,-1.20185167898973E-16));
#6739=DIRECTION('',(0.,-1.,0.));
#6740=DIRECTION('',(1.,0.,1.20185167898973E-16));
#6741=DIRECTION('center_axis',(-0.866025403784439,0.,-0.5));
#6742=DIRECTION('ref_axis',(0.5,0.,-0.866025403784439));
#6743=DIRECTION('',(-0.5,0.,0.866025403784439));
#6744=DIRECTION('',(0.,-1.,0.));
#6745=DIRECTION('',(0.5,0.,-0.866025403784439));
#6746=DIRECTION('center_axis',(-0.866025403784439,0.,0.5));
#6747=DIRECTION('ref_axis',(-0.5,0.,-0.866025403784439));
#6748=DIRECTION('',(0.5,0.,0.866025403784439));
#6749=DIRECTION('',(0.,-1.,0.));
#6750=DIRECTION('',(-0.5,0.,-0.866025403784439));
#6751=DIRECTION('center_axis',(-2.40370335797945E-16,0.,1.));
#6752=DIRECTION('ref_axis',(-1.,0.,-2.40370335797945E-16));
#6753=DIRECTION('',(1.,0.,2.40370335797945E-16));
#6754=DIRECTION('',(0.,-1.,0.));
#6755=DIRECTION('',(-1.,0.,-2.40370335797945E-16));
#6756=DIRECTION('center_axis',(0.866025403784439,0.,0.5));
#6757=DIRECTION('ref_axis',(-0.5,0.,0.866025403784439));
#6758=DIRECTION('',(0.5,0.,-0.866025403784439));
#6759=DIRECTION('',(-0.5,0.,0.866025403784439));
#6760=DIRECTION('center_axis',(0.,1.,0.));
#6761=DIRECTION('ref_axis',(1.,0.,0.));
#6762=DIRECTION('center_axis',(0.,-1.,0.));
#6763=DIRECTION('ref_axis',(0.,0.,-1.));
#8190=CARTESIAN_POINT('',(0.,0.,0.));
#8191=CARTESIAN_POINT('Origin',(0.375,0.5,0.));
#8192=CARTESIAN_POINT('',(-0.375,0.5,-4.59242549680257E-17));
#8193=CARTESIAN_POINT('Origin',(0.,0.5,0.));
#8194=CARTESIAN_POINT('Origin',(0.,0.475,0.));
#8195=CARTESIAN_POINT('',(-0.425,0.45,-5.20474889637625E-17));
#8196=CARTESIAN_POINT('Origin',(0.,0.45,0.));
#8197=CARTESIAN_POINT('',(-0.4,0.475,-4.89858719658941E-17));
#8198=CARTESIAN_POINT('Origin',(0.,0.24,0.));
#8199=CARTESIAN_POINT('',(-0.425,0.0299999999999998,-5.20474889637625E-17));
#8200=CARTESIAN_POINT('Origin',(0.,0.0299999999999998,0.));
#8201=CARTESIAN_POINT('',(-0.425,0.24,-5.20474889637625E-17));
#8202=CARTESIAN_POINT('Origin',(0.,0.0150000000000001,0.));
#8203=CARTESIAN_POINT('',(-0.395,4.85722573273506E-17,-4.83735485663204E-17));
#8204=CARTESIAN_POINT('Origin',(0.,0.,0.));
#8205=CARTESIAN_POINT('',(-0.41,0.0150000000000001,-5.02105187650415E-17));
#8206=CARTESIAN_POINT('Origin',(0.27,0.,0.));
#8207=CARTESIAN_POINT('',(-0.27,0.,-3.30654635769785E-17));
#8208=CARTESIAN_POINT('Origin',(0.,0.,0.));
#8209=CARTESIAN_POINT('Origin',(0.,-0.02,0.));
#8210=CARTESIAN_POINT('',(-0.24505,-0.0498999999999999,3.00099698131059E-17));
#8211=CARTESIAN_POINT('Origin',(0.,-0.0498999999999999,0.));
#8212=CARTESIAN_POINT('',(-0.26,-0.02,-3.18408167778312E-17));
#8213=CARTESIAN_POINT('Origin',(0.,-0.995,0.));
#8214=CARTESIAN_POINT('',(-0.24505,-1.95495,3.00099698131059E-17));
#8215=CARTESIAN_POINT('Origin',(0.,-1.95495,0.));
#8216=CARTESIAN_POINT('',(-0.24505,-0.995,-3.00099698131059E-17));
#8217=CARTESIAN_POINT('Origin',(0.,-1.975,0.));
#8218=CARTESIAN_POINT('',(-0.2,-2.,-2.44929359829471E-17));
#8219=CARTESIAN_POINT('Origin',(0.,-2.,0.));
#8220=CARTESIAN_POINT('',(-0.225,-1.975,-2.75545529808154E-17));
#8221=CARTESIAN_POINT('Origin',(0.,-2.,0.));
#8222=CARTESIAN_POINT('Origin',(0.115470053837925,-0.5,-0.2));
#8223=CARTESIAN_POINT('',(0.23094010767585,-0.5,0.));
#8224=CARTESIAN_POINT('',(0.115470053837925,-0.5,-0.2));
#8225=CARTESIAN_POINT('',(0.23094010767585,-0.5,0.));
#8226=CARTESIAN_POINT('',(0.115470053837925,-0.8,-0.2));
#8227=CARTESIAN_POINT('',(0.115470053837925,-0.5,-0.2));
#8228=CARTESIAN_POINT('',(0.23094010767585,-0.8,0.));
#8229=CARTESIAN_POINT('',(0.23094010767585,-0.8,0.));
#8230=CARTESIAN_POINT('',(0.23094010767585,-0.5,0.));
#8231=CARTESIAN_POINT('Origin',(-0.115470053837925,-0.5,-0.2));
#8232=CARTESIAN_POINT('',(-0.115470053837925,-0.5,-0.2));
#8233=CARTESIAN_POINT('',(0.115470053837925,-0.5,-0.2));
#8234=CARTESIAN_POINT('',(-0.115470053837925,-0.8,-0.2));
#8235=CARTESIAN_POINT('',(-0.115470053837925,-0.5,-0.2));
#8236=CARTESIAN_POINT('',(0.115470053837925,-0.8,-0.2));
#8237=CARTESIAN_POINT('Origin',(-0.23094010767585,-0.5,-2.77555756156289E-17));
#8238=CARTESIAN_POINT('',(-0.23094010767585,-0.5,-2.82820063659975E-17));
#8239=CARTESIAN_POINT('',(-0.115470053837925,-0.5,-0.2));
#8240=CARTESIAN_POINT('',(-0.23094010767585,-0.8,-2.77555756156289E-17));
#8241=CARTESIAN_POINT('',(-0.23094010767585,-0.5,-2.82820063659975E-17));
#8242=CARTESIAN_POINT('',(-0.115470053837925,-0.8,-0.2));
#8243=CARTESIAN_POINT('Origin',(-0.115470053837925,-0.5,0.2));
#8244=CARTESIAN_POINT('',(-0.115470053837925,-0.5,0.2));
#8245=CARTESIAN_POINT('',(-0.23094010767585,-0.5,-2.82820063659975E-17));
#8246=CARTESIAN_POINT('',(-0.115470053837925,-0.8,0.2));
#8247=CARTESIAN_POINT('',(-0.115470053837925,-0.5,0.2));
#8248=CARTESIAN_POINT('',(-0.23094010767585,-0.8,-2.82820063659975E-17));
#8249=CARTESIAN_POINT('Origin',(0.115470053837925,-0.5,0.2));
#8250=CARTESIAN_POINT('',(0.115470053837925,-0.5,0.2));
#8251=CARTESIAN_POINT('',(-0.115470053837925,-0.5,0.2));
#8252=CARTESIAN_POINT('',(0.115470053837925,-0.8,0.2));
#8253=CARTESIAN_POINT('',(0.115470053837925,-0.5,0.2));
#8254=CARTESIAN_POINT('',(-0.115470053837925,-0.8,0.2));
#8255=CARTESIAN_POINT('Origin',(0.23094010767585,-0.5,0.));
#8256=CARTESIAN_POINT('',(0.115470053837925,-0.5,0.2));
#8257=CARTESIAN_POINT('',(0.115470053837925,-0.8,0.2));
#8258=CARTESIAN_POINT('Origin',(0.,-0.5,0.));
#8259=CARTESIAN_POINT('Origin',(0.,-0.8,0.));
#9049=UNCERTAINTY_MEASURE_WITH_UNIT(LENGTH_MEASURE(0.001),#9103,
'DISTANCE_ACCURACY_VALUE',
'Maximum model space distance between geometric entities at asserted c
onnectivities');
#9069=UNCERTAINTY_MEASURE_WITH_UNIT(LENGTH_MEASURE(0.001),#9103,
'DISTANCE_ACCURACY_VALUE',
'Maximum model space distance between geometric entities at asserted c
onnectivities');
#9082=(
GEOMETRIC_REPRESENTATION_CONTEXT(3)
GLOBAL_UNCERTAINTY_ASSIGNED_CONTEXT((#9049))
GLOBAL_UNIT_ASSIGNED_CONTEXT((#9103,#9105,#9106))
REPRESENTATION_CONTEXT('','3D')
);
#9102=(
GEOMETRIC_REPRESENTATION_CONTEXT(3)
GLOBAL_UNCERTAINTY_ASSIGNED_CONTEXT((#9069))
GLOBAL_UNIT_ASSIGNED_CONTEXT((#9103,#9105,#9106))
REPRESENTATION_CONTEXT('','3D')
);
#9103=(
LENGTH_UNIT()
NAMED_UNIT(*)
SI_UNIT(.CENTI.,.METRE.)
);
#9105=(
NAMED_UNIT(*)
PLANE_ANGLE_UNIT()
SI_UNIT($,.RADIAN.)
);
#9106=(
NAMED_UNIT(*)
SI_UNIT($,.STERADIAN.)
SOLID_ANGLE_UNIT()
);
#9119=SHAPE_DEFINITION_REPRESENTATION(#9151,#9239);
#9151=PRODUCT_DEFINITION_SHAPE('',$,#9272);
#9239=SHAPE_REPRESENTATION('',(#5568),#9082);
#9259=PRODUCT_DEFINITION_CONTEXT('part definition',#9357,'design');
#9272=PRODUCT_DEFINITION('Cap Screw - M5x20','Cap Screw - M5x20',#9304,
#9259);
#9304=PRODUCT_DEFINITION_FORMATION('',$,#9371);
#9357=APPLICATION_CONTEXT(
'Core Data for Automotive Mechanical Design Process');
#9358=PRODUCT_CONTEXT('part definition',#9357,'mechanical');
#9371=PRODUCT('Cap Screw - M5x20','Cap Screw - M5x20',
'Cap Screw - M5x20',(#9358));
#9461=COLOUR_RGB('Black',0.12,0.14,0.17);
#9462=FILL_AREA_STYLE_COLOUR('',#9461);
#9463=FILL_AREA_STYLE('',(#9462));
#9464=SURFACE_STYLE_FILL_AREA(#9463);
#9465=SURFACE_SIDE_STYLE('',(#9464));
#9466=SURFACE_STYLE_USAGE(.BOTH.,#9465);
#9467=PRESENTATION_STYLE_ASSIGNMENT((#9466));
ENDSEC;
END-ISO-10303-21;
